ISO-10303-21;
HEADER;
/* Generated by software containing ST-Developer
 * from STEP Tools, Inc. (www.steptools.com) 
 */
/* OPTION: using custom renumber hook */

FILE_DESCRIPTION(
/* description */ ('STEP AP242 Edition 2', 'CAx-IF Rec.Pracs.---Representation and Presentation of Product Manufa
cturing Information (PMI)---4.0---2014-10-13', 'CAx-IF Rec.Pracs.---3D Tessellated Geometry---0.4---2014-09-14', '2;1', 'CAx-IF Rec.Pracs.---User Defined Attributes---1.5---2016-08-15'),
/* implementation_level */ '2;1');

FILE_NAME(
/* name */ 'Part 2__PD10220.step',
/* time_stamp */ '2026-10-09T13:59:33Z',
/* author */ (''),
/* organization */ (''),
/* preprocessor_version */ 'ST-DEVELOPER v20',
/* originating_system */ 'ONSHAPE BY PTC INC, 1.221',
/* authorisation */ '  ');

FILE_SCHEMA (('AP242_MANAGED_MODEL_BASED_3D_ENGINEERING_MIM_LF { 1 0 10303 442 3 1 4 }'));
ENDSEC;

DATA;
#272=LINE('',#9799,#556);
#273=LINE('',#9803,#557);
#274=LINE('',#9807,#558);
#275=LINE('',#9813,#559);
#276=LINE('',#9817,#560);
#277=LINE('',#9818,#561);
#556=VECTOR('',#8060,1.);
#557=VECTOR('',#8063,1.);
#558=VECTOR('',#8068,1.);
#559=VECTOR('',#8075,1.);
#560=VECTOR('',#8080,1.);
#561=VECTOR('',#8081,1.);
#679=SHAPE_REPRESENTATION_RELATIONSHIP('','',#5698,#693);
#693=ADVANCED_BREP_SHAPE_REPRESENTATION('',(#5666),#10152);
#764=PLANE('',#6370);
#765=PLANE('',#6371);
#766=PLANE('',#6373);
#2088=ORIENTED_EDGE('',*,*,#2981,.F.);
#2089=ORIENTED_EDGE('',*,*,#2982,.F.);
#2090=ORIENTED_EDGE('',*,*,#2983,.T.);
#2091=ORIENTED_EDGE('',*,*,#2984,.T.);
#2092=ORIENTED_EDGE('',*,*,#2985,.F.);
#2093=ORIENTED_EDGE('',*,*,#2986,.F.);
#2094=ORIENTED_EDGE('',*,*,#2987,.T.);
#2095=ORIENTED_EDGE('',*,*,#2982,.T.);
#2096=ORIENTED_EDGE('',*,*,#2988,.F.);
#2097=ORIENTED_EDGE('',*,*,#2989,.F.);
#2098=ORIENTED_EDGE('',*,*,#2990,.T.);
#2099=ORIENTED_EDGE('',*,*,#2986,.T.);
#2100=ORIENTED_EDGE('',*,*,#2991,.F.);
#2101=ORIENTED_EDGE('',*,*,#2984,.F.);
#2102=ORIENTED_EDGE('',*,*,#2992,.T.);
#2103=ORIENTED_EDGE('',*,*,#2989,.T.);
#2104=ORIENTED_EDGE('',*,*,#2993,.T.);
#2105=ORIENTED_EDGE('',*,*,#2983,.F.);
#2106=ORIENTED_EDGE('',*,*,#2987,.F.);
#2107=ORIENTED_EDGE('',*,*,#2990,.F.);
#2108=ORIENTED_EDGE('',*,*,#2992,.F.);
#2109=ORIENTED_EDGE('',*,*,#2994,.F.);
#2110=ORIENTED_EDGE('',*,*,#2981,.T.);
#2111=ORIENTED_EDGE('',*,*,#2991,.T.);
#2112=ORIENTED_EDGE('',*,*,#2988,.T.);
#2113=ORIENTED_EDGE('',*,*,#2985,.T.);
#2114=ORIENTED_EDGE('',*,*,#2993,.F.);
#2115=ORIENTED_EDGE('',*,*,#2994,.T.);
#2981=EDGE_CURVE('',#3555,#3556,#4038,.T.);
#2982=EDGE_CURVE('',#3557,#3555,#272,.T.);
#2983=EDGE_CURVE('',#3557,#3558,#4039,.T.);
#2984=EDGE_CURVE('',#3558,#3556,#273,.T.);
#2985=EDGE_CURVE('',#3559,#3555,#4040,.T.);
#2986=EDGE_CURVE('',#3560,#3559,#274,.T.);
#2987=EDGE_CURVE('',#3560,#3557,#4041,.T.);
#2988=EDGE_CURVE('',#3561,#3559,#4042,.T.);
#2989=EDGE_CURVE('',#3562,#3561,#275,.T.);
#2990=EDGE_CURVE('',#3562,#3560,#4043,.T.);
#2991=EDGE_CURVE('',#3556,#3561,#276,.T.);
#2992=EDGE_CURVE('',#3558,#3562,#277,.T.);
#2993=EDGE_CURVE('',#3563,#3563,#4044,.T.);
#2994=EDGE_CURVE('',#3564,#3564,#4045,.T.);
#3555=VERTEX_POINT('',#9797);
#3556=VERTEX_POINT('',#9798);
#3557=VERTEX_POINT('',#9800);
#3558=VERTEX_POINT('',#9802);
#3559=VERTEX_POINT('',#9806);
#3560=VERTEX_POINT('',#9808);
#3561=VERTEX_POINT('',#9812);
#3562=VERTEX_POINT('',#9814);
#3563=VERTEX_POINT('',#9821);
#3564=VERTEX_POINT('',#9824);
#4038=CIRCLE('',#6362,0.051);
#4039=CIRCLE('',#6363,0.051);
#4040=CIRCLE('',#6365,0.002);
#4041=CIRCLE('',#6366,0.002);
#4042=CIRCLE('',#6368,0.049);
#4043=CIRCLE('',#6369,0.049);
#4044=CIRCLE('',#6372,0.0015);
#4045=CIRCLE('',#6374,0.0015);
#4452=EDGE_LOOP('',(#2088,#2089,#2090,#2091));
#4453=EDGE_LOOP('',(#2092,#2093,#2094,#2095));
#4454=EDGE_LOOP('',(#2096,#2097,#2098,#2099));
#4455=EDGE_LOOP('',(#2100,#2101,#2102,#2103));
#4456=EDGE_LOOP('',(#2104));
#4457=EDGE_LOOP('',(#2105,#2106,#2107,#2108));
#4458=EDGE_LOOP('',(#2109));
#4459=EDGE_LOOP('',(#2110,#2111,#2112,#2113));
#4460=EDGE_LOOP('',(#2114));
#4461=EDGE_LOOP('',(#2115));
#4900=FACE_BOUND('',#4452,.T.);
#4901=FACE_BOUND('',#4453,.T.);
#4902=FACE_BOUND('',#4454,.T.);
#4903=FACE_BOUND('',#4455,.T.);
#4904=FACE_BOUND('',#4456,.T.);
#4905=FACE_BOUND('',#4457,.T.);
#4906=FACE_BOUND('',#4458,.T.);
#4907=FACE_BOUND('',#4459,.T.);
#4908=FACE_BOUND('',#4460,.T.);
#4909=FACE_BOUND('',#4461,.T.);
#5189=CYLINDRICAL_SURFACE('',#6361,0.051);
#5190=CYLINDRICAL_SURFACE('',#6364,0.002);
#5191=CYLINDRICAL_SURFACE('',#6367,0.049);
#5192=CYLINDRICAL_SURFACE('',#6375,0.0015);
#5471=ADVANCED_FACE('',(#4900),#5189,.T.);
#5472=ADVANCED_FACE('',(#4901),#5190,.T.);
#5473=ADVANCED_FACE('',(#4902),#5191,.F.);
#5474=ADVANCED_FACE('',(#4903),#764,.T.);
#5475=ADVANCED_FACE('',(#4904,#4905),#765,.F.);
#5476=ADVANCED_FACE('',(#4906,#4907),#766,.T.);
#5477=ADVANCED_FACE('',(#4908,#4909),#5192,.F.);
#5547=CLOSED_SHELL('',(#5471,#5472,#5473,#5474,#5475,#5476,#5477));
#5561=STYLED_ITEM('',(#5575),#5666);
#5575=PRESENTATION_STYLE_ASSIGNMENT((#5589));
#5589=SURFACE_STYLE_USAGE(.BOTH.,#5603);
#5603=SURFACE_SIDE_STYLE('',(#5617));
#5617=SURFACE_STYLE_FILL_AREA(#5631);
#5631=FILL_AREA_STYLE('',(#5645));
#5645=FILL_AREA_STYLE_COLOUR('',#5656);
#5656=COLOUR_RGB('', 0.40784314, 0.44705882, 0.49803922);
#5666=MANIFOLD_SOLID_BREP('Part 2',#5547);
#5682=SHAPE_DEFINITION_REPRESENTATION(#10197,#5698);
#5698=SHAPE_REPRESENTATION('Part 2',(#5704),#10152);
#5704=AXIS2_PLACEMENT_3D('',#8391,#6505,#6506);
#6361=AXIS2_PLACEMENT_3D('',#9795,#8056,#8057);
#6362=AXIS2_PLACEMENT_3D('',#9796,#8058,#8059);
#6363=AXIS2_PLACEMENT_3D('',#9801,#8061,#8062);
#6364=AXIS2_PLACEMENT_3D('',#9804,#8064,#8065);
#6365=AXIS2_PLACEMENT_3D('',#9805,#8066,#8067);
#6366=AXIS2_PLACEMENT_3D('',#9809,#8069,#8070);
#6367=AXIS2_PLACEMENT_3D('',#9810,#8071,#8072);
#6368=AXIS2_PLACEMENT_3D('',#9811,#8073,#8074);
#6369=AXIS2_PLACEMENT_3D('',#9815,#8076,#8077);
#6370=AXIS2_PLACEMENT_3D('',#9816,#8078,#8079);
#6371=AXIS2_PLACEMENT_3D('',#9819,#8082,#8083);
#6372=AXIS2_PLACEMENT_3D('',#9820,#8084,#8085);
#6373=AXIS2_PLACEMENT_3D('',#9822,#8086,#8087);
#6374=AXIS2_PLACEMENT_3D('',#9823,#8088,#8089);
#6375=AXIS2_PLACEMENT_3D('',#9825,#8090,#8091);
#6505=DIRECTION('',(0.,0.,1.));
#6506=DIRECTION('',(1.,0.,0.));
#8056=DIRECTION('',(1.,0.,0.));
#8057=DIRECTION('',(0.,0.,-1.));
#8058=DIRECTION('',(1.,0.,0.));
#8059=DIRECTION('',(0.,0.,-1.));
#8060=DIRECTION('',(1.,0.,0.));
#8061=DIRECTION('',(1.,0.,0.));
#8062=DIRECTION('',(0.,0.,-1.));
#8063=DIRECTION('',(1.,0.,0.));
#8064=DIRECTION('',(1.,0.,0.));
#8065=DIRECTION('',(0.,0.,-1.));
#8066=DIRECTION('',(1.,0.,0.));
#8067=DIRECTION('',(0.,0.,-1.));
#8068=DIRECTION('',(1.,0.,0.));
#8069=DIRECTION('',(1.,0.,0.));
#8070=DIRECTION('',(0.,0.,-1.));
#8071=DIRECTION('',(1.,0.,0.));
#8072=DIRECTION('',(0.,0.,-1.));
#8073=DIRECTION('',(-1.,0.,0.));
#8074=DIRECTION('',(0.,0.,-1.));
#8075=DIRECTION('',(1.,0.,0.));
#8076=DIRECTION('',(-1.,0.,0.));
#8077=DIRECTION('',(0.,0.,-1.));
#8078=DIRECTION('',(0.,1.,0.));
#8079=DIRECTION('',(0.,0.,1.));
#8080=DIRECTION('',(0.,0.,1.));
#8081=DIRECTION('',(0.,0.,1.));
#8082=DIRECTION('',(1.,0.,0.));
#8083=DIRECTION('',(0.,0.,-1.));
#8084=DIRECTION('',(1.,0.,0.));
#8085=DIRECTION('',(0.,0.,-1.));
#8086=DIRECTION('',(1.,0.,0.));
#8087=DIRECTION('',(0.,0.,-1.));
#8088=DIRECTION('',(1.,0.,0.));
#8089=DIRECTION('',(0.,0.,-1.));
#8090=DIRECTION('',(1.,0.,0.));
#8091=DIRECTION('',(0.,0.,-1.));
#8391=CARTESIAN_POINT('',(0.,0.,0.));
#9795=CARTESIAN_POINT('',(-0.001,0.,0.));
#9796=CARTESIAN_POINT('',(0.001,0.,0.));
#9797=CARTESIAN_POINT('',(0.001,0.00174902830165781,-0.05097));
#9798=CARTESIAN_POINT('',(0.001,0.005,-0.0507543101617981));
#9799=CARTESIAN_POINT('',(-0.001,0.00174902830165781,-0.05097));
#9800=CARTESIAN_POINT('',(-0.001,0.00174902830165781,-0.05097));
#9801=CARTESIAN_POINT('',(-0.001,0.,0.));
#9802=CARTESIAN_POINT('',(-0.001,0.005,-0.0507543101617981));
#9803=CARTESIAN_POINT('',(-0.001,0.005,-0.0507543101617981));
#9804=CARTESIAN_POINT('',(-0.001,0.,-0.05));
#9805=CARTESIAN_POINT('',(0.001,0.,-0.05));
#9806=CARTESIAN_POINT('',(0.001,0.00171438035453047,-0.04897));
#9807=CARTESIAN_POINT('',(-0.001,0.00171438035453047,-0.04897));
#9808=CARTESIAN_POINT('',(-0.001,0.00171438035453047,-0.04897));
#9809=CARTESIAN_POINT('',(-0.001,0.,-0.05));
#9810=CARTESIAN_POINT('',(-0.001,0.,0.));
#9811=CARTESIAN_POINT('',(0.001,0.,0.));
#9812=CARTESIAN_POINT('',(0.001,0.005,-0.0487442304278158));
#9813=CARTESIAN_POINT('',(-0.001,0.005,-0.0487442304278158));
#9814=CARTESIAN_POINT('',(-0.001,0.005,-0.0487442304278158));
#9815=CARTESIAN_POINT('',(-0.001,0.,0.));
#9816=CARTESIAN_POINT('',(-0.001,0.005,-0.0487442304278158));
#9817=CARTESIAN_POINT('',(0.001,0.005,-0.0487442304278158));
#9818=CARTESIAN_POINT('',(-0.001,0.005,-0.0487442304278158));
#9819=CARTESIAN_POINT('',(-0.001,0.,0.));
#9820=CARTESIAN_POINT('',(-0.001,0.,-0.05));
#9821=CARTESIAN_POINT('',(-0.001,0.,-0.0515));
#9822=CARTESIAN_POINT('',(0.001,0.,0.));
#9823=CARTESIAN_POINT('',(0.001,0.,-0.05));
#9824=CARTESIAN_POINT('',(0.001,0.,-0.0515));
#9825=CARTESIAN_POINT('',(-0.001,0.,-0.05));
#10141=MECHANICAL_DESIGN_GEOMETRIC_PRESENTATION_REPRESENTATION('',(#5561),#10142);
#10142=(
GEOMETRIC_REPRESENTATION_CONTEXT(3)
GLOBAL_UNCERTAINTY_ASSIGNED_CONTEXT((#10158))
GLOBAL_UNIT_ASSIGNED_CONTEXT((#10176,#10175,#10174))
REPRESENTATION_CONTEXT('MAS-674','TOP_LEVEL_ASSEMBLY_PART')
);
#10152=(
GEOMETRIC_REPRESENTATION_CONTEXT(3)
GLOBAL_UNCERTAINTY_ASSIGNED_CONTEXT((#10168))
GLOBAL_UNIT_ASSIGNED_CONTEXT((#10176,#10175,#10174))
REPRESENTATION_CONTEXT('Part 2','COMPONENT_PART')
);
#10158=UNCERTAINTY_MEASURE_WITH_UNIT(LENGTH_MEASURE(1.E-8),#10176,
'DISTANCE_ACCURACY_VALUE','Maximum Tolerance applied to model');
#10168=UNCERTAINTY_MEASURE_WITH_UNIT(LENGTH_MEASURE(1.E-8),#10176,
'DISTANCE_ACCURACY_VALUE','Maximum Tolerance applied to model');
#10174=(
NAMED_UNIT(*)
SI_UNIT($,.STERADIAN.)
SOLID_ANGLE_UNIT()
);
#10175=(
NAMED_UNIT(*)
PLANE_ANGLE_UNIT()
SI_UNIT($,.RADIAN.)
);
#10176=(
LENGTH_UNIT()
NAMED_UNIT(*)
SI_UNIT($,.METRE.)
);
#10197=PRODUCT_DEFINITION_SHAPE('','',#10220);
#10220=PRODUCT_DEFINITION('','',#10252,#10236);
#10236=PRODUCT_DEFINITION_CONTEXT('',#10323,'design');
#10252=PRODUCT_DEFINITION_FORMATION_WITH_SPECIFIED_SOURCE('','',#10284,
 .NOT_KNOWN.);
#10284=PRODUCT('Part 2','Part 2','Part 2',(#10316));
#10316=PRODUCT_CONTEXT('',#10323,'mechanical');
#10323=APPLICATION_CONTEXT('managed model based 3d engineering');
ENDSEC;
END-ISO-10303-21;
